ISO-10303-21;
HEADER;
/* Generated by software containing ST-Developer
 * from STEP Tools, Inc. (www.steptools.com) 
 */

FILE_DESCRIPTION(
/* description */ ('PAT-080'),
/* implementation_level */ '2;1');

FILE_NAME(
/* name */ 'Bonded pad (1).step',
/* time_stamp */ '2026-10-29T20:13:47-07:00',
/* author */ (''),
/* organization */ (''),
/* preprocessor_version */ 'ST-DEVELOPER v20.2',
/* originating_system */ 'Autodesk Translation Framework v15.17.0.0',
/* authorisation */ '');

FILE_SCHEMA (('AUTOMOTIVE_DESIGN { 1 0 10303 214 3 1 1 }'));
ENDSEC;

DATA;
#10=MECHANICAL_DESIGN_GEOMETRIC_PRESENTATION_REPRESENTATION('',(#248),#6878);
#210=SHAPE_REPRESENTATION_RELATIONSHIP('SRR','None',#6966,#229);
#229=ADVANCED_BREP_SHAPE_REPRESENTATION('',(#267),#6861);
#248=STYLED_ITEM('',(#7143),#267);
#267=MANIFOLD_SOLID_BREP('Body1',#3864);
#369=PLANE('',#4122);
#370=PLANE('',#4123);
#371=PLANE('',#4124);
#372=PLANE('',#4125);
#373=PLANE('',#4126);
#374=PLANE('',#4127);
#516=FACE_OUTER_BOUND('',#750,.T.);
#517=FACE_OUTER_BOUND('',#751,.T.);
#518=FACE_OUTER_BOUND('',#752,.T.);
#519=FACE_OUTER_BOUND('',#753,.T.);
#520=FACE_OUTER_BOUND('',#754,.T.);
#521=FACE_OUTER_BOUND('',#755,.T.);
#750=EDGE_LOOP('',(#2680,#2681,#2682,#2683));
#751=EDGE_LOOP('',(#2684,#2685,#2686,#2687));
#752=EDGE_LOOP('',(#2688,#2689,#2690,#2691));
#753=EDGE_LOOP('',(#2692,#2693,#2694,#2695));
#754=EDGE_LOOP('',(#2696,#2697,#2698,#2699));
#755=EDGE_LOOP('',(#2700,#2701,#2702,#2703));
#1056=LINE('',#5812,#1371);
#1057=LINE('',#5814,#1372);
#1058=LINE('',#5816,#1373);
#1059=LINE('',#5817,#1374);
#1060=LINE('',#5820,#1375);
#1061=LINE('',#5822,#1376);
#1062=LINE('',#5823,#1377);
#1063=LINE('',#5826,#1378);
#1064=LINE('',#5828,#1379);
#1065=LINE('',#5829,#1380);
#1066=LINE('',#5831,#1381);
#1067=LINE('',#5832,#1382);
#1371=VECTOR('',#4620,1.);
#1372=VECTOR('',#4621,1.);
#1373=VECTOR('',#4622,1.);
#1374=VECTOR('',#4623,1.);
#1375=VECTOR('',#4626,1.);
#1376=VECTOR('',#4627,1.);
#1377=VECTOR('',#4628,1.);
#1378=VECTOR('',#4631,1.);
#1379=VECTOR('',#4632,1.);
#1380=VECTOR('',#4633,1.);
#1381=VECTOR('',#4636,1.);
#1382=VECTOR('',#4637,1.);
#1834=VERTEX_POINT('',#5810);
#1835=VERTEX_POINT('',#5811);
#1836=VERTEX_POINT('',#5813);
#1837=VERTEX_POINT('',#5815);
#1838=VERTEX_POINT('',#5819);
#1839=VERTEX_POINT('',#5821);
#1840=VERTEX_POINT('',#5825);
#1841=VERTEX_POINT('',#5827);
#2163=EDGE_CURVE('',#1834,#1835,#1056,.T.);
#2164=EDGE_CURVE('',#1835,#1836,#1057,.T.);
#2165=EDGE_CURVE('',#1837,#1836,#1058,.T.);
#2166=EDGE_CURVE('',#1834,#1837,#1059,.T.);
#2167=EDGE_CURVE('',#1838,#1834,#1060,.T.);
#2168=EDGE_CURVE('',#1839,#1837,#1061,.T.);
#2169=EDGE_CURVE('',#1838,#1839,#1062,.T.);
#2170=EDGE_CURVE('',#1840,#1838,#1063,.T.);
#2171=EDGE_CURVE('',#1841,#1839,#1064,.T.);
#2172=EDGE_CURVE('',#1840,#1841,#1065,.T.);
#2173=EDGE_CURVE('',#1835,#1840,#1066,.T.);
#2174=EDGE_CURVE('',#1836,#1841,#1067,.T.);
#2680=ORIENTED_EDGE('',*,*,#2163,.T.);
#2681=ORIENTED_EDGE('',*,*,#2164,.T.);
#2682=ORIENTED_EDGE('',*,*,#2165,.F.);
#2683=ORIENTED_EDGE('',*,*,#2166,.F.);
#2684=ORIENTED_EDGE('',*,*,#2167,.T.);
#2685=ORIENTED_EDGE('',*,*,#2166,.T.);
#2686=ORIENTED_EDGE('',*,*,#2168,.F.);
#2687=ORIENTED_EDGE('',*,*,#2169,.F.);
#2688=ORIENTED_EDGE('',*,*,#2170,.T.);
#2689=ORIENTED_EDGE('',*,*,#2169,.T.);
#2690=ORIENTED_EDGE('',*,*,#2171,.F.);
#2691=ORIENTED_EDGE('',*,*,#2172,.F.);
#2692=ORIENTED_EDGE('',*,*,#2173,.T.);
#2693=ORIENTED_EDGE('',*,*,#2172,.T.);
#2694=ORIENTED_EDGE('',*,*,#2174,.F.);
#2695=ORIENTED_EDGE('',*,*,#2164,.F.);
#2696=ORIENTED_EDGE('',*,*,#2174,.T.);
#2697=ORIENTED_EDGE('',*,*,#2171,.T.);
#2698=ORIENTED_EDGE('',*,*,#2168,.T.);
#2699=ORIENTED_EDGE('',*,*,#2165,.T.);
#2700=ORIENTED_EDGE('',*,*,#2173,.F.);
#2701=ORIENTED_EDGE('',*,*,#2163,.F.);
#2702=ORIENTED_EDGE('',*,*,#2167,.F.);
#2703=ORIENTED_EDGE('',*,*,#2170,.F.);
#3652=ADVANCED_FACE('',(#516),#369,.T.);
#3653=ADVANCED_FACE('',(#517),#370,.T.);
#3654=ADVANCED_FACE('',(#518),#371,.T.);
#3655=ADVANCED_FACE('',(#519),#372,.T.);
#3656=ADVANCED_FACE('',(#520),#373,.T.);
#3657=ADVANCED_FACE('',(#521),#374,.F.);
#3864=CLOSED_SHELL('',(#3652,#3653,#3654,#3655,#3656,#3657));
#4121=AXIS2_PLACEMENT_3D('',#5808,#4616,#4617);
#4122=AXIS2_PLACEMENT_3D('',#5809,#4618,#4619);
#4123=AXIS2_PLACEMENT_3D('',#5818,#4624,#4625);
#4124=AXIS2_PLACEMENT_3D('',#5824,#4629,#4630);
#4125=AXIS2_PLACEMENT_3D('',#5830,#4634,#4635);
#4126=AXIS2_PLACEMENT_3D('',#5833,#4638,#4639);
#4127=AXIS2_PLACEMENT_3D('',#5834,#4640,#4641);
#4616=DIRECTION('axis',(0.,0.,1.));
#4617=DIRECTION('refdir',(1.,0.,0.));
#4618=DIRECTION('center_axis',(0.,1.,0.));
#4619=DIRECTION('ref_axis',(-1.,0.,0.));
#4620=DIRECTION('',(-1.,0.,0.));
#4621=DIRECTION('',(0.,0.,1.));
#4622=DIRECTION('',(-1.,0.,0.));
#4623=DIRECTION('',(0.,0.,1.));
#4624=DIRECTION('center_axis',(1.,0.,0.));
#4625=DIRECTION('ref_axis',(0.,1.,0.));
#4626=DIRECTION('',(0.,1.,0.));
#4627=DIRECTION('',(0.,1.,0.));
#4628=DIRECTION('',(0.,0.,1.));
#4629=DIRECTION('center_axis',(0.,-1.,0.));
#4630=DIRECTION('ref_axis',(1.,0.,0.));
#4631=DIRECTION('',(1.,0.,0.));
#4632=DIRECTION('',(1.,0.,0.));
#4633=DIRECTION('',(0.,0.,1.));
#4634=DIRECTION('center_axis',(-1.,0.,0.));
#4635=DIRECTION('ref_axis',(0.,-1.,0.));
#4636=DIRECTION('',(0.,-1.,0.));
#4637=DIRECTION('',(0.,-1.,0.));
#4638=DIRECTION('center_axis',(0.,0.,1.));
#4639=DIRECTION('ref_axis',(1.,0.,0.));
#4640=DIRECTION('center_axis',(0.,0.,1.));
#4641=DIRECTION('ref_axis',(1.,0.,0.));
#5808=CARTESIAN_POINT('',(0.,0.,0.));
#5809=CARTESIAN_POINT('Origin',(14.,5.,-0.3));
#5810=CARTESIAN_POINT('',(14.,5.,-0.3));
#5811=CARTESIAN_POINT('',(12.,5.,-0.3));
#5812=CARTESIAN_POINT('',(14.,5.,-0.3));
#5813=CARTESIAN_POINT('',(12.,5.,0.));
#5814=CARTESIAN_POINT('',(12.,5.,-0.3));
#5815=CARTESIAN_POINT('',(14.,5.,0.));
#5816=CARTESIAN_POINT('',(14.,5.,0.));
#5817=CARTESIAN_POINT('',(14.,5.,-0.3));
#5818=CARTESIAN_POINT('Origin',(14.,-5.,-0.3));
#5819=CARTESIAN_POINT('',(14.,-5.,-0.3));
#5820=CARTESIAN_POINT('',(14.,-5.,-0.3));
#5821=CARTESIAN_POINT('',(14.,-5.,0.));
#5822=CARTESIAN_POINT('',(14.,-5.,0.));
#5823=CARTESIAN_POINT('',(14.,-5.,-0.3));
#5824=CARTESIAN_POINT('Origin',(12.,-5.,-0.3));
#5825=CARTESIAN_POINT('',(12.,-5.,-0.3));
#5826=CARTESIAN_POINT('',(12.,-5.,-0.3));
#5827=CARTESIAN_POINT('',(12.,-5.,0.));
#5828=CARTESIAN_POINT('',(12.,-5.,0.));
#5829=CARTESIAN_POINT('',(12.,-5.,-0.3));
#5830=CARTESIAN_POINT('Origin',(12.,5.,-0.3));
#5831=CARTESIAN_POINT('',(12.,5.,-0.3));
#5832=CARTESIAN_POINT('',(12.,5.,0.));
#5833=CARTESIAN_POINT('Origin',(13.,0.,0.));
#5834=CARTESIAN_POINT('Origin',(13.,0.,-0.3));
#6840=UNCERTAINTY_MEASURE_WITH_UNIT(LENGTH_MEASURE(0.001),#6879,
'DISTANCE_ACCURACY_VALUE',
'Maximum model space distance between geometric entities at asserted c
onnectivities');
#6857=UNCERTAINTY_MEASURE_WITH_UNIT(LENGTH_MEASURE(0.001),#6879,
'DISTANCE_ACCURACY_VALUE',
'Maximum model space distance between geometric entities at asserted c
onnectivities');
#6861=(
GEOMETRIC_REPRESENTATION_CONTEXT(3)
GLOBAL_UNCERTAINTY_ASSIGNED_CONTEXT((#6840))
GLOBAL_UNIT_ASSIGNED_CONTEXT((#6879,#6881,#6882))
REPRESENTATION_CONTEXT('','3D')
);
#6878=(
GEOMETRIC_REPRESENTATION_CONTEXT(3)
GLOBAL_UNCERTAINTY_ASSIGNED_CONTEXT((#6857))
GLOBAL_UNIT_ASSIGNED_CONTEXT((#6879,#6881,#6882))
REPRESENTATION_CONTEXT('','3D')
);
#6879=(
LENGTH_UNIT()
NAMED_UNIT(*)
SI_UNIT(.CENTI.,.METRE.)
);
#6881=(
NAMED_UNIT(*)
PLANE_ANGLE_UNIT()
SI_UNIT($,.RADIAN.)
);
#6882=(
NAMED_UNIT(*)
SI_UNIT($,.STERADIAN.)
SOLID_ANGLE_UNIT()
);
#6886=SHAPE_DEFINITION_REPRESENTATION(#6906,#6966);
#6906=PRODUCT_DEFINITION_SHAPE('',$,#6987);
#6966=SHAPE_REPRESENTATION('',(#4121),#6861);
#6983=PRODUCT_DEFINITION_CONTEXT('part definition',#7045,'design');
#6987=PRODUCT_DEFINITION('Bonded pad (1)','Bonded pad (1)',#7007,
#6983);
#7007=PRODUCT_DEFINITION_FORMATION('',$,#7050);
#7045=APPLICATION_CONTEXT(
'Core Data for Automotive Mechanical Design Process');
#7046=PRODUCT_CONTEXT('part definition',#7045,'mechanical');
#7050=PRODUCT('Bonded pad (1)','Bonded pad (1)','Bonded pad (1)',(#7046));
#7137=COLOUR_RGB('Off White',0.89,0.88,0.83);
#7138=FILL_AREA_STYLE_COLOUR('',#7137);
#7139=FILL_AREA_STYLE('',(#7138));
#7140=SURFACE_STYLE_FILL_AREA(#7139);
#7141=SURFACE_SIDE_STYLE('',(#7140));
#7142=SURFACE_STYLE_USAGE(.BOTH.,#7141);
#7143=PRESENTATION_STYLE_ASSIGNMENT((#7142));
ENDSEC;
END-ISO-10303-21;
